ISO-10303-21;
HEADER;
FILE_DESCRIPTION (('STEP AP203'),
    '1' );
FILE_NAME ('1602p_c_43.step',
    '2026-10-31T14:11:27',
    ( '' ),
    ( '' ),
    'SwSTEP 2.0',
    'SolidWorks 2024',
    '' );
FILE_SCHEMA (( 'AUTOMOTIVE_DESIGN' ));
ENDSEC;

DATA;
#217=AXIS2_PLACEMENT_3D ( 'NONE', #15090, #20672, #22793 ) ;
#304=CARTESIAN_POINT ( 'NONE',  ( 58.49563186522070168, 17.70675969991879839, -15.25462000000050011 ) ) ;
#415=DIRECTION ( 'NONE',  ( 1.000000000000000000, 0.000000000000000000, 0.000000000000000000 ) ) ;
#423=DIRECTION ( 'NONE',  ( 0.9286452767786566032, 1.871119812896368998E-17, -0.3709689338970208472 ) ) ;
#483=VERTEX_POINT ( 'NONE', #6751 ) ;
#505=LINE ( 'NONE', #20807, #5051 ) ;
#616=ORIENTED_EDGE ( 'NONE', *, *, #17227, .T. ) ;
#682=AXIS2_PLACEMENT_3D ( 'NONE', #22326, #20327, #20442 ) ;
#707=ADVANCED_FACE ( 'NONE', ( #3989 ), #12448, .T. ) ;
#736=CARTESIAN_POINT ( 'NONE',  ( 37.48968750243700043, 22.68571848161319693, -13.00000000000049916 ) ) ;
#750=ORIENTED_EDGE ( 'NONE', *, *, #5274, .F. ) ;
#767=ORIENTED_EDGE ( 'NONE', *, *, #1383, .F. ) ;
#815=VERTEX_POINT ( 'NONE', #14791 ) ;
#879=DIRECTION ( 'NONE',  ( 0.1997366180463766849, 0.8426774492125652660, -0.5000000000000004441 ) ) ;
#886=VERTEX_POINT ( 'NONE', #6361 ) ;
#906=CONICAL_SURFACE ( 'NONE', #14198, 1.154700538379250796, 1.047197551196598297 ) ;
#928=VERTEX_POINT ( 'NONE', #15265 ) ;
#943=LINE ( 'NONE', #13788, #20944 ) ;
#946=PLANE ( 'NONE',  #6699 ) ;
#956=CARTESIAN_POINT ( 'NONE',  ( 58.25686728443101003, 17.76335315678745630, -10.50000000000049916 ) ) ;
#991=DIRECTION ( 'NONE',  ( -0.1153179901961009640, -0.4865200521429018377, -0.8660254037844385966 ) ) ;
#1031=CYLINDRICAL_SURFACE ( 'NONE', #10387, 4.250000000000001776 ) ;
#1032=ORIENTED_EDGE ( 'NONE', *, *, #1810, .T. ) ;
#1040=EDGE_CURVE ( 'NONE', #22846, #5938, #22362, .T. ) ;
#1043=CARTESIAN_POINT ( 'NONE',  ( 35.35837847849400362, 22.00420084508149898, -11.00000000000049916 ) ) ;
#1112=ADVANCED_FACE ( 'NONE', ( #10642 ), #2941, .T. ) ;
#1139=EDGE_CURVE ( 'NONE', #5418, #22740, #19622, .T. ) ;
#1166=EDGE_LOOP ( 'NONE', ( #4398, #7483, #5209, #13554 ) ) ;
#1176=FACE_OUTER_BOUND ( 'NONE', #12104, .T. ) ;
#1231=AXIS2_PLACEMENT_3D ( 'NONE', #21907, #5416, #1725 ) ;
#1265=AXIS2_PLACEMENT_3D ( 'NONE', #1825, #3618, #5398 ) ;
#1271=ORIENTED_EDGE ( 'NONE', *, *, #12894, .F. ) ;
#1383=EDGE_CURVE ( 'NONE', #3573, #22846, #17735, .T. ) ;
#1402=ORIENTED_EDGE ( 'NONE', *, *, #23017, .T. ) ;
#1432=FACE_BOUND ( 'NONE', #22637, .T. ) ;
#1459=CARTESIAN_POINT ( 'NONE',  ( 33.94234173009040489, 21.44981837135919989, -12.50000000000050093 ) ) ;
#1473=LINE ( 'NONE', #7312, #6614 ) ;
#1505=DIRECTION ( 'NONE',  ( 0.9730401042858036753, -0.2306359803922028995, -5.432877459303547669E-17 ) ) ;
#1510=PRODUCT_DEFINITION_FORMATION_WITH_SPECIFIED_SOURCE ( 'ANY', '', #10832, .NOT_KNOWN. ) ;
#1529=LINE ( 'NONE', #23269, #4299 ) ;
#1584=CARTESIAN_POINT ( 'NONE',  ( 34.89491389100810181, 23.30074776265909975, -13.00000000000049916 ) ) ;
#1602=CARTESIAN_POINT ( 'NONE',  ( 34.03002896453733683, 19.65184737158733341, -13.00000000000049916 ) ) ;
#1621=CARTESIAN_POINT ( 'NONE',  ( 39.27359436029428963, 22.26288585089417538, -17.25000000000050093 ) ) ;
#1675=( BOUNDED_CURVE ( )  B_SPLINE_CURVE ( 2, ( #6572, #15462, #19165 ),
 .UNSPECIFIED., .F., .F. ) 
 B_SPLINE_CURVE_WITH_KNOTS ( ( 3, 3 ),
 ( 0.000000000000000000, 0.2336872276155859962 ),
 .UNSPECIFIED. ) 
 CURVE ( )  GEOMETRIC_REPRESENTATION_ITEM ( )  RATIONAL_B_SPLINE_CURVE ( ( 1.000000000000000000, 1.154700538379249908, 1.000000000000000000 ) ) 
 REPRESENTATION_ITEM ( '' )  );
#1689=DIRECTION ( 'NONE',  ( -0.4865200521429013936, 0.1153179901961013387, -0.8660254037844388186 ) ) ;
#1725=DIRECTION ( 'NONE',  ( -0.9730401042858036753, 0.2306359803922023999, -1.110223024625155524E-17 ) ) ;
#1726=ORIENTED_EDGE ( 'NONE', *, *, #10182, .T. ) ;
#1758=DIRECTION ( 'NONE',  ( 0.000000000000000000, -1.000000000000000000, 9.355573283744330345E-16 ) ) ;
#1810=EDGE_CURVE ( 'NONE', #11102, #23420, #2675, .T. ) ;
#1819=CARTESIAN_POINT ( 'NONE',  ( 34.89491389100810181, 23.30074776265909975, -13.00000000000049916 ) ) ;
#1825=CARTESIAN_POINT ( 'NONE',  ( 34.40839383886520153, 23.41606575285519654, -13.00000000000049916 ) ) ;
#1865=ADVANCED_FACE ( 'NONE', ( #18905 ), #18840, .F. ) ;
#1878=DIRECTION ( 'NONE',  ( -2.829953705592110306E-16, -9.355573283744330345E-16, -1.000000000000000000 ) ) ;
#1886=AXIS2_PLACEMENT_3D ( 'NONE', #1819, #4928, #19419 ) ;
#1910=AXIS2_PLACEMENT_3D ( 'NONE', #6136, #20855, #6018 ) ;
#1996=ADVANCED_FACE ( 'NONE', ( #17244 ), #946, .F. ) ;
#2034=ORIENTED_EDGE ( 'NONE', *, *, #6517, .F. ) ;
#2048=ADVANCED_FACE ( 'NONE', ( #1176 ), #12477, .T. ) ;
#2178=VECTOR ( 'NONE', #6582, 999.9999999999998863 ) ;
#2179=CIRCLE ( 'NONE', #18110, 4.250000000000000000 ) ;
#2210=AXIS2_PLACEMENT_3D ( 'NONE', #14856, #22101, #13211 ) ;
#2215=DIRECTION ( 'NONE',  ( 0.1997366180463769070, 0.8426774492125652660, 0.5000000000000003331 ) ) ;
#2234=CARTESIAN_POINT ( 'NONE',  ( 37.01481097301073930, 22.79827665208023291, -11.00000000000049560 ) ) ;
#2308=CARTESIAN_POINT ( 'NONE',  ( 39.94748832170330388, 24.67242251356951144, -13.00000000000049916 ) ) ;
#2312=PLANE ( 'NONE',  #17147 ) ;
#2368=VERTEX_POINT ( 'NONE', #7430 ) ;
#2440=CARTESIAN_POINT ( 'NONE',  ( 37.10730959030829723, 23.96304573415810069, -11.00000000000049916 ) ) ;
#2525=ORIENTED_EDGE ( 'NONE', *, *, #8870, .F. ) ;
#2561=VERTEX_POINT ( 'NONE', #2440 ) ;
#2569=CARTESIAN_POINT ( 'NONE',  ( 0.000000000000000000, 0.000000000000000000, 0.000000000000000000 ) ) ;
#2592=VERTEX_POINT ( 'NONE', #2308 ) ;
#2607=DIRECTION ( 'NONE',  ( 0.000000000000000000, 1.000000000000000000, 0.000000000000000000 ) ) ;
#2638=DIRECTION ( 'NONE',  ( 0.000000000000000000, 0.000000000000000000, 1.000000000000000000 ) ) ;
#2675=CIRCLE ( 'NONE', #16693, 4.250000000000001776 ) ;
#2717=DIRECTION ( 'NONE',  ( 0.9730401042858035643, -0.2306359803922028717, -5.432877459303547053E-17 ) ) ;
#2765=ORIENTED_EDGE ( 'NONE', *, *, #16902, .T. ) ;
#2792=CIRCLE ( 'NONE', #5823, 2.500000000000000444 ) ;
#2803=CIRCLE ( 'NONE', #19063, 0.09999999999999939493 ) ;
#2836=FACE_OUTER_BOUND ( 'NONE', #16588, .T. ) ;
#2890=LINE ( 'NONE', #4435, #2178 ) ;
#2900=ADVANCED_FACE ( 'NONE', ( #12516 ), #9061, .F. ) ;
#2941=TOROIDAL_SURFACE ( 'NONE', #17356, 3.750000000000000000, 0.5000000000000000000 ) ;
#2974=EDGE_CURVE ( 'NONE', #3517, #17960, #15537, .T. ) ;
#3008=DIRECTION ( 'NONE',  ( -0.2306359803922028440, -0.9730401042858034533, -4.307366329831518561E-32 ) ) ;
#3015=CARTESIAN_POINT ( 'NONE',  ( 37.56481403710107969, 24.44795204016911327, -12.00000000000050271 ) ) ;
#3040=ORIENTED_EDGE ( 'NONE', *, *, #15651, .F. ) ;
#3046=DIRECTION ( 'NONE',  ( 6.124378941433959925E-17, 0.000000000000000000, 1.000000000000000000 ) ) ;
#3063=CARTESIAN_POINT ( 'NONE',  ( 37.37362508103680625, 25.08661566644150298, -13.00000000000049916 ) ) ;
#3146=VECTOR ( 'NONE', #15542, 999.9999999999998863 ) ;
#3200=ORIENTED_EDGE ( 'NONE', *, *, #1810, .F. ) ;
#3217=DIRECTION ( 'NONE',  ( -0.9730401042858035643, 0.2306359803922028717, 5.667427308550587516E-17 ) ) ;
#3254=VERTEX_POINT ( 'NONE', #10338 ) ;
#3286=EDGE_CURVE ( 'NONE', #8780, #483, #11171, .T. ) ;
#3445=TOROIDAL_SURFACE ( 'NONE', #1910, 2.600000000000000089, 0.1000000000000000056 ) ;
#3462=DIRECTION ( 'NONE',  ( 0.000000000000000000, 1.000000000000000000, 0.000000000000000000 ) ) ;
#3480=CARTESIAN_POINT ( 'NONE',  ( 36.15732495067950225, 25.37491064193179824, -13.00000000000049916 ) ) ;
#3517=VERTEX_POINT ( 'NONE', #4122 ) ;
#3573=VERTEX_POINT ( 'NONE', #20635 ) ;
#3618=DIRECTION ( 'NONE',  ( 0.9730401042858036753, -0.2306359803922031493, -5.959266323858673745E-17 ) ) ;
#3794=ORIENTED_EDGE ( 'NONE', *, *, #2974, .F. ) ;
#3803=DIRECTION ( 'NONE',  ( 0.9730401042858036753, -0.2306359803922031493, -5.432877459303553216E-17 ) ) ;
#3847=DIRECTION ( 'NONE',  ( -0.4865200521429014491, 0.1153179901961012555, 0.8660254037844388186 ) ) ;
#3926=VERTEX_POINT ( 'NONE', #18365 ) ;
#3967=ADVANCED_FACE ( 'NONE', ( #15128 ), #2312, .F. ) ;
#3989=FACE_OUTER_BOUND ( 'NONE', #13509, .T. ) ;
#4053=CIRCLE ( 'NONE', #17729, 2.009240000000000581 ) ;
#4122=CARTESIAN_POINT ( 'NONE',  ( 34.67470932959370344, 24.53963568513860238, -15.00000000000049916 ) ) ;
#4190=DIRECTION ( 'NONE',  ( 0.2306359803922028995, 0.9730401042858036753, -9.756037151021835575E-16 ) ) ;
#4224=DIRECTION ( 'NONE',  ( -0.9730401042858035643, 0.2306359803922028717, 5.667427308550587516E-17 ) ) ;
#4270=CIRCLE ( 'NONE', #9201, 2.500000000000000444 ) ;
#4299=VECTOR ( 'NONE', #17712, 999.9999999999998863 ) ;
#4312=CARTESIAN_POINT ( 'NONE',  ( 39.27359436029428963, 22.26288585089417538, -8.750000000000499156 ) ) ;
#4316=CARTESIAN_POINT ( 'NONE',  ( 39.37089837072279863, 22.23982225285499936, -13.00000000000049916 ) ) ;
#4398=ORIENTED_EDGE ( 'NONE', *, *, #6234, .F. ) ;
#4435=CARTESIAN_POINT ( 'NONE',  ( 49.97703550743810297, 19.72589006657999988, -10.50000000000049916 ) ) ;
#4469=EDGE_CURVE ( 'NONE', #2592, #23382, #4270, .T. ) ;
#4480=EDGE_CURVE ( 'NONE', #18764, #2592, #17919, .T. ) ;
#4497=ORIENTED_EDGE ( 'NONE', *, *, #20411, .T. ) ;
#4557=CARTESIAN_POINT ( 'NONE',  ( 58.49563186522070168, 17.70675969991879839, -10.74538000000049820 ) ) ;
#4583=ADVANCED_FACE ( 'NONE', ( #21264, #1432 ), #4661, .T. ) ;
#4616=AXIS2_PLACEMENT_3D ( 'NONE', #15186, #6651, #2607 ) ;
#4661=PLANE ( 'NONE',  #6544 ) ;
#4753=AXIS2_PLACEMENT_3D ( 'NONE', #18878, #17076, #7946 ) ;
#4914=DIRECTION ( 'NONE',  ( 0.9730401042858035643, -0.2306359803922028717, -5.959266323858677443E-17 ) ) ;
#4928=DIRECTION ( 'NONE',  ( -0.9730401042858036753, 0.2306359803922031493, 5.432877459303543355E-17 ) ) ;
#4940=ORIENTED_EDGE ( 'NONE', *, *, #13911, .F. ) ;
#4944=ORIENTED_EDGE ( 'NONE', *, *, #5037, .F. ) ;
#4952=ORIENTED_EDGE ( 'NONE', *, *, #8689, .T. ) ;
#5006=CARTESIAN_POINT ( 'NONE',  ( 39.27359436029429673, 22.26288585089420025, -16.37500000000050093 ) ) ;
#5037=EDGE_CURVE ( 'NONE', #3254, #9785, #11007, .T. ) ;
#5051=VECTOR ( 'NONE', #4190, 999.9999999999998863 ) ;
#5096=ORIENTED_EDGE ( 'NONE', *, *, #20411, .F. ) ;
#5185=DIRECTION ( 'NONE',  ( -0.2306359803922028995, -0.9730401042858035643, 3.648592655857288816E-32 ) ) ;
#5196=AXIS2_PLACEMENT_3D ( 'NONE', #20799, #20333, #22334 ) ;
#5209=ORIENTED_EDGE ( 'NONE', *, *, #18986, .F. ) ;
#5246=CARTESIAN_POINT ( 'NONE',  ( 36.57467860885130051, 21.71590586959130320, -15.00000000000049916 ) ) ;
#5253=LINE ( 'NONE', #18084, #9115 ) ;
#5274=EDGE_CURVE ( 'NONE', #17960, #11172, #16670, .T. ) ;
#5322=VECTOR ( 'NONE', #7206, 1000.000000000000114 ) ;
#5346=FACE_OUTER_BOUND ( 'NONE', #18860, .T. ) ;
#5398=DIRECTION ( 'NONE',  ( 0.000000000000000000, 0.000000000000000000, 1.000000000000000000 ) ) ;
#5400=EDGE_CURVE ( 'NONE', #17785, #8770, #11408, .T. ) ;
#5416=DIRECTION ( 'NONE',  ( -0.1997366180463769070, -0.8426774492125652660, 0.5000000000000002220 ) ) ;
#5418=VERTEX_POINT ( 'NONE', #18482 ) ;
#5517=CARTESIAN_POINT ( 'NONE',  ( 35.89100945995100034, 24.25134070964839950, -11.00000000000049916 ) ) ;
#5553=ORIENTED_EDGE ( 'NONE', *, *, #21146, .F. ) ;
#5563=FACE_OUTER_BOUND ( 'NONE', #8371, .T. ) ;
#5581=ORIENTED_EDGE ( 'NONE', *, *, #6344, .F. ) ;
#5660=LINE ( 'NONE', #304, #10727 ) ;
#5684=( GEOMETRIC_REPRESENTATION_CONTEXT ( 3 ) GLOBAL_UNCERTAINTY_ASSIGNED_CONTEXT ( ( #23423 ) ) GLOBAL_UNIT_ASSIGNED_CONTEXT ( ( #7374, #18413, #22181 ) ) REPRESENTATION_CONTEXT ( 'NONE', 'WORKASPACE' ) );
#5699=CARTESIAN_POINT ( 'NONE',  ( 39.97055191974253319, 24.76972652399809149, -13.00000000000049916 ) ) ;
#5708=CIRCLE ( 'NONE', #19743, 0.1000000000000028644 ) ;
#5718=DIRECTION ( 'NONE',  ( 0.1153179901961009640, 0.4865200521429018377, 0.8660254037844385966 ) ) ;
#5735=VECTOR ( 'NONE', #13587, 1000.000000000000114 ) ;
#5777=AXIS2_PLACEMENT_3D ( 'NONE', #11432, #13312, #22087 ) ;
#5787=VECTOR ( 'NONE', #991, 1000.000000000000114 ) ;
#5822=ORIENTED_EDGE ( 'NONE', *, *, #1139, .T. ) ;
#5823=AXIS2_PLACEMENT_3D ( 'NONE', #16443, #21902, #7091 ) ;
#5846=FACE_OUTER_BOUND ( 'NONE', #16348, .T. ) ;
#5882=AXIS2_PLACEMENT_3D ( 'NONE', #10825, #1878, #1758 ) ;
#5938=VERTEX_POINT ( 'NONE', #21526 ) ;
#6018=DIRECTION ( 'NONE',  ( -0.2306359803922028440, -0.9730401042858034533, -4.307366329831518561E-32 ) ) ;
#6080=DIRECTION ( 'NONE',  ( -0.9730401042858035643, 0.2306359803922028717, 6.126766849694256332E-17 ) ) ;
#6136=CARTESIAN_POINT ( 'NONE',  ( 39.37089837072279863, 22.23982225285499936, -13.00000000000049916 ) ) ;
#6185=TOROIDAL_SURFACE ( 'NONE', #17935, 3.750000000000000000, 0.5000000000000000000 ) ;
#6234=EDGE_CURVE ( 'NONE', #8780, #928, #1675, .T. ) ;
#6235=DIRECTION ( 'NONE',  ( 0.000000000000000000, 0.000000000000000000, -1.000000000000000000 ) ) ;
#6256=CARTESIAN_POINT ( 'NONE',  ( 34.27523609350100031, 22.85428078671350249, -11.00000000000049916 ) ) ;
#6263=( BOUNDED_CURVE ( )  B_SPLINE_CURVE ( 2, ( #5246, #14735, #9287 ),
 .UNSPECIFIED., .F., .F. ) 
 B_SPLINE_CURVE_WITH_KNOTS ( ( 3, 3 ),
 ( 0.000000000000000000, 0.2336872276155859962 ),
 .UNSPECIFIED. ) 
 CURVE ( )  GEOMETRIC_REPRESENTATION_ITEM ( )  RATIONAL_B_SPLINE_CURVE ( ( 1.000000000000000000, 1.154700538379259900, 1.000000000000000000 ) ) 
 REPRESENTATION_ITEM ( '' )  );
#6312=DIRECTION ( 'NONE',  ( 0.000000000000000000, 0.000000000000000000, 1.000000000000000000 ) ) ;
#6344=EDGE_CURVE ( 'NONE', #2592, #14730, #2803, .T. ) ;
#6351=CARTESIAN_POINT ( 'NONE',  ( 39.27359436029429673, 22.26288585089420025, -13.00000000000049916 ) ) ;
#6361=CARTESIAN_POINT ( 'NONE',  ( 58.73439644601031517, 17.65016624305016890, -15.00924000000053660 ) ) ;
#6416=DIRECTION ( 'NONE',  ( 0.000000000000000000, 0.5102823824563427202, -0.8600069128528436968 ) ) ;
#6442=DIRECTION ( 'NONE',  ( -0.9730401042858036753, 0.2306359803922031493, 5.432877459303543355E-17 ) ) ;
#6467=AXIS2_PLACEMENT_3D ( 'NONE', #17823, #2215, #423 ) ;
#6517=EDGE_CURVE ( 'NONE', #23382, #22935, #17595, .T. ) ;
#6523=DIRECTION ( 'NONE',  ( 0.9730401042858035643, -0.2306359803922028717, -5.432877459303547053E-17 ) ) ;
#6533=ORIENTED_EDGE ( 'NONE', *, *, #8370, .F. ) ;
#6544=AXIS2_PLACEMENT_3D ( 'NONE', #5006, #10490, #20916 ) ;
#6572=CARTESIAN_POINT ( 'NONE',  ( 36.30836311812279860, 20.59233593730780143, -13.00000000000049916 ) ) ;
#6579=DIRECTION ( 'NONE',  ( 0.000000000000000000, 0.000000000000000000, 1.000000000000000000 ) ) ;
#6582=DIRECTION ( 'NONE',  ( 0.9730401042858036753, -0.2306359803922028995, -5.432877459303547669E-17 ) ) ;
#6614=VECTOR ( 'NONE', #3847, 1000.000000000000114 ) ;
#6636=ORIENTED_EDGE ( 'NONE', *, *, #7362, .F. ) ;
#6651=DIRECTION ( 'NONE',  ( -8.623081276789554834E-17, -1.054188326053478339E-16, -1.000000000000000000 ) ) ;
#6695=EDGE_CURVE ( 'NONE', #22846, #11102, #943, .T. ) ;
#6699=AXIS2_PLACEMENT_3D ( 'NONE', #15437, #22674, #6416 ) ;
#6710=VECTOR ( 'NONE', #5718, 1000.000000000000114 ) ;
#6716=CARTESIAN_POINT ( 'NONE',  ( 37.10730959030829723, 23.96304573415810069, -11.00000000000049916 ) ) ;
#6751=CARTESIAN_POINT ( 'NONE',  ( 33.87576285740820481, 21.16892588828840260, -13.00000000000049916 ) ) ;
#6802=ORIENTED_EDGE ( 'NONE', *, *, #14162, .T. ) ;
#6860=ORIENTED_EDGE ( 'NONE', *, *, #6695, .F. ) ;
#6909=LINE ( 'NONE', #23146, #14302 ) ;
#6990=PLANE ( 'NONE',  #14501 ) ;
#7045=ORIENTED_EDGE ( 'NONE', *, *, #10690, .F. ) ;
#7091=DIRECTION ( 'NONE',  ( 0.000000000000000000, 0.000000000000000000, 1.000000000000000000 ) ) ;
#7184=DIRECTION ( 'NONE',  ( 0.9730401042858035643, -0.2306359803922028717, -5.959266323858677443E-17 ) ) ;
#7206=DIRECTION ( 'NONE',  ( -0.1153179901961009640, -0.4865200521429018377, 0.8660254037844385966 ) ) ;
#7256=CARTESIAN_POINT ( 'NONE',  ( 58.49563186522070168, 17.70675969991879839, -13.00000000000049916 ) ) ;
#7312=CARTESIAN_POINT ( 'NONE',  ( 37.48968750243700043, 22.68571848161319693, -11.84529946162124858 ) ) ;
#7345=EDGE_LOOP ( 'NONE', ( #6636, #23158 ) ) ;
#7362=EDGE_CURVE ( 'NONE', #22740, #5418, #10774, .T. ) ;
#7374=( LENGTH_UNIT ( ) NAMED_UNIT ( * ) SI_UNIT ( .MILLI., .METRE. ) );
#7430=CARTESIAN_POINT ( 'NONE',  ( 34.89491389100810181, 23.30074776265910330, -17.25000000000050093 ) ) ;
#7483=ORIENTED_EDGE ( 'NONE', *, *, #3286, .T. ) ;
#7493=DIRECTION ( 'NONE',  ( 0.000000000000000000, 0.000000000000000000, 1.000000000000000000 ) ) ;
#7566=ORIENTED_EDGE ( 'NONE', *, *, #7751, .T. ) ;
#7607=ORIENTED_EDGE ( 'NONE', *, *, #14997, .F. ) ;
#7662=ORIENTED_EDGE ( 'NONE', *, *, #15469, .F. ) ;
#7664=CARTESIAN_POINT ( 'NONE',  ( 37.10730959030829723, 23.96304573415810069, -15.00000000000049916 ) ) ;
#7751=EDGE_CURVE ( 'NONE', #2368, #23420, #1529, .T. ) ;
#7764=DIRECTION ( 'NONE',  ( 0.000000000000000000, 0.000000000000000000, 1.000000000000000000 ) ) ;
#7782=CARTESIAN_POINT ( 'NONE',  ( 34.94102482032229773, 25.66320561742200113, -13.00000000000049916 ) ) ;
#7785=ORIENTED_EDGE ( 'NONE', *, *, #15908, .T. ) ;
#7787=( BOUNDED_CURVE ( )  B_SPLINE_CURVE ( 2, ( #6716, #3015, #15609 ),
 .UNSPECIFIED., .F., .T. ) 
 B_SPLINE_CURVE_WITH_KNOTS ( ( 3, 3 ),
 ( 0.000000000000000000, 0.2336872276155859962 ),
 .UNSPECIFIED. ) 
 CURVE ( )  GEOMETRIC_REPRESENTATION_ITEM ( )  RATIONAL_B_SPLINE_CURVE ( ( 1.000000000000000000, 1.154700538379259900, 1.000000000000000000 ) ) 
 REPRESENTATION_ITEM ( '' )  );
#7869=CARTESIAN_POINT ( 'NONE',  ( 39.37089837072279863, 22.23982225285499936, -13.00000000000049916 ) ) ;
#7932=ORIENTED_EDGE ( 'NONE', *, *, #14403, .F. ) ;
#7946=DIRECTION ( 'NONE',  ( 0.000000000000000000, 0.000000000000000000, 1.000000000000000000 ) ) ;
#7949=CARTESIAN_POINT ( 'NONE',  ( 36.84099409957970295, 22.83947580187469839, -13.00000000000049916 ) ) ;
#8037=EDGE_CURVE ( 'NONE', #18213, #2561, #11274, .T. ) ;
#8068=ORIENTED_EDGE ( 'NONE', *, *, #14162, .F. ) ;
#8132=ADVANCED_FACE ( 'NONE', ( #2836 ), #1031, .T. ) ;
#8139=CARTESIAN_POINT ( 'NONE',  ( 58.73439644601030096, 17.65016624305009785, -13.00000000000049916 ) ) ;
#8150=CARTESIAN_POINT ( 'NONE',  ( 35.89100945995100034, 24.25134070964839950, -15.00000000000049916 ) ) ;
#8207=( BOUNDED_CURVE ( )  B_SPLINE_CURVE ( 2, ( #3063, #19219, #10333 ),
 .UNSPECIFIED., .F., .F. ) 
 B_SPLINE_CURVE_WITH_KNOTS ( ( 3, 3 ),
 ( 0.000000000000000000, 0.2336872276155859962 ),
 .UNSPECIFIED. ) 
 CURVE ( )  GEOMETRIC_REPRESENTATION_ITEM ( )  RATIONAL_B_SPLINE_CURVE ( ( 1.000000000000000000, 1.154700538379259900, 1.000000000000000000 ) ) 
 REPRESENTATION_ITEM ( '' )  );
#8370=EDGE_CURVE ( 'NONE', #22329, #17785, #8207, .T. ) ;
#8371=EDGE_LOOP ( 'NONE', ( #10114, #4497, #15023, #7607, #21225 ) ) ;
#8409=ORIENTED_EDGE ( 'NONE', *, *, #5274, .T. ) ;
#8428=DIRECTION ( 'NONE',  ( 0.000000000000000000, 0.000000000000000000, -1.000000000000000000 ) ) ;
#8569=DIRECTION ( 'NONE',  ( 0.9730401042858035643, -0.2306359803922028717, -5.959266323858674978E-17 ) ) ;
#8573=SHAPE_DEFINITION_REPRESENTATION ( #17637, #22194 ) ;
#8593=PLANE ( 'NONE',  #5882 ) ;
#8689=EDGE_CURVE ( 'NONE', #11172, #20160, #9720, .T. ) ;
#8754=CARTESIAN_POINT ( 'NONE',  ( 34.89491389100810181, 23.30074776265909975, -13.00000000000049916 ) ) ;
#8770=VERTEX_POINT ( 'NONE', #20975 ) ;
#8780=VERTEX_POINT ( 'NONE', #17416 ) ;
#8802=EDGE_LOOP ( 'NONE', ( #5581, #15519, #18650, #1726, #20890 ) ) ;
#8870=EDGE_CURVE ( 'NONE', #19293, #18213, #1473, .T. ) ;
#8873=CIRCLE ( 'NONE', #10410, 0.5000000000000004441 ) ;
#8987=CARTESIAN_POINT ( 'NONE',  ( 39.37089837072280574, 22.23982225285502068, -10.50000000000049916 ) ) ;
#9061=PLANE ( 'NONE',  #16930 ) ;
#9115=VECTOR ( 'NONE', #20088, 1000.000000000000114 ) ;
#9201=AXIS2_PLACEMENT_3D ( 'NONE', #4316, #18453, #22113 ) ;
#9217=ORIENTED_EDGE ( 'NONE', *, *, #1040, .T. ) ;
#9247=ADVANCED_FACE ( 'NONE', ( #17023 ), #906, .F. ) ;
#9287=CARTESIAN_POINT ( 'NONE',  ( 36.30836311812279860, 20.59233593730780143, -13.00000000000049916 ) ) ;
#9433=CIRCLE ( 'NONE', #2210, 4.250000000000000000 ) ;
#9493=EDGE_CURVE ( 'NONE', #483, #23152, #5253, .T. ) ;
#9590=AXIS2_PLACEMENT_3D ( 'NONE', #7869, #6080, #2638 ) ;
#9636=ORIENTED_EDGE ( 'NONE', *, *, #10961, .F. ) ;
#9720=LINE ( 'NONE', #6256, #14921 ) ;
#9724=CARTESIAN_POINT ( 'NONE',  ( 38.77124482170307118, 19.70991798171191078, -13.00000000000049916 ) ) ;
#9736=ORIENTED_EDGE ( 'NONE', *, *, #22553, .F. ) ;
#9755=CARTESIAN_POINT ( 'NONE',  ( 37.10730959030829723, 23.96304573415810069, -15.00000000000049916 ) ) ;
#9785=VERTEX_POINT ( 'NONE', #956 ) ;
#9786=VERTEX_POINT ( 'NONE', #17362 ) ;
#9789=ORIENTED_EDGE ( 'NONE', *, *, #18986, .T. ) ;
#9848=MANIFOLD_SOLID_BREP ( 'Imported1', #22396 ) ;
#9850=CARTESIAN_POINT ( 'NONE',  ( 38.79430841974229338, 19.80722199214049084, -13.00000000000049916 ) ) ;
#9892=CARTESIAN_POINT ( 'NONE',  ( 34.67470932959370344, 24.53963568513860238, -11.00000000000049916 ) ) ;
#9935=ADVANCED_FACE ( 'NONE', ( #14805 ), #12375, .F. ) ;
#9972=ORIENTED_EDGE ( 'NONE', *, *, #17227, .F. ) ;
#10055=FACE_OUTER_BOUND ( 'NONE', #18599, .T. ) ;
#10097=ADVANCED_FACE ( 'NONE', ( #22522 ), #3445, .F. ) ;
#10114=ORIENTED_EDGE ( 'NONE', *, *, #5400, .F. ) ;
#10143=VECTOR ( 'NONE', #20286, 999.9999999999998863 ) ;
#10154=AXIS2_PLACEMENT_3D ( 'NONE', #16292, #16076, #14283 ) ;
#10182=EDGE_CURVE ( 'NONE', #22935, #3926, #5708, .T. ) ;
#10333=CARTESIAN_POINT ( 'NONE',  ( 37.10730959030829723, 23.96304573415810069, -15.00000000000049916 ) ) ;
#10338=CARTESIAN_POINT ( 'NONE',  ( 58.25686728443101003, 17.76335315678745630, -15.50000000000049916 ) ) ;
#10387=AXIS2_PLACEMENT_3D ( 'NONE', #7949, #2717, #13179 ) ;
#10410=AXIS2_PLACEMENT_3D ( 'NONE', #1602, #20014, #23450 ) ;
#10435=EDGE_CURVE ( 'NONE', #8770, #9786, #15479, .T. ) ;
#10490=DIRECTION ( 'NONE',  ( 0.9730401042858035643, -0.2306359803922028717, -5.959266323858674978E-17 ) ) ;
#10642=FACE_OUTER_BOUND ( 'NONE', #13266, .T. ) ;
#10690=EDGE_CURVE ( 'NONE', #815, #9785, #13127, .T. ) ;
#10727=VECTOR ( 'NONE', #20285, 1000.000000000000114 ) ;
#10771=DIRECTION ( 'NONE',  ( -0.2306359803922028995, -0.9730401042858035643, 3.648592655857288816E-32 ) ) ;
#10774=CIRCLE ( 'NONE', #1265, 3.750000000000000000 ) ;
#10825=CARTESIAN_POINT ( 'NONE',  ( 34.67470932959370344, 24.53963568513860238, -15.00000000000049916 ) ) ;
#10832=PRODUCT ( '1602p_c_43', '1602p_c_43', '', ( #13667 ) ) ;
#10957=EDGE_LOOP ( 'NONE', ( #12440, #14877, #12220, #16147, #22955 ) ) ;
#10961=EDGE_CURVE ( 'NONE', #886, #815, #13931, .T. ) ;
#11007=CIRCLE ( 'NONE', #19717, 2.500000000000000444 ) ;
#11083=DIRECTION ( 'NONE',  ( 0.000000000000000000, 0.000000000000000000, -1.000000000000000000 ) ) ;
#11102=VERTEX_POINT ( 'NONE', #4312 ) ;
#11142=CARTESIAN_POINT ( 'NONE',  ( 37.13840842239409312, 23.31972727237319631, -15.00000000000051159 ) ) ;
#11165=ORIENTED_EDGE ( 'NONE', *, *, #11185, .F. ) ;
#11171=LINE ( 'NONE', #18391, #10143 ) ;
#11172=VERTEX_POINT ( 'NONE', #9892 ) ;
#11185=EDGE_CURVE ( 'NONE', #14730, #3926, #15061, .T. ) ;
#11206=ORIENTED_EDGE ( 'NONE', *, *, #5037, .T. ) ;
#11274=( BOUNDED_CURVE ( )  B_SPLINE_CURVE ( 2, ( #2234, #16260, #14079 ),
 .UNSPECIFIED., .F., .F. ) 
 B_SPLINE_CURVE_WITH_KNOTS ( ( 3, 3 ),
 ( 0.1168436138077847686, 0.2336872276155859962 ),
 .UNSPECIFIED. ) 
 CURVE ( )  GEOMETRIC_REPRESENTATION_ITEM ( )  RATIONAL_B_SPLINE_CURVE ( ( 1.077350269189624843, 1.077350269189630394, 1.000000000000000000 ) ) 
 REPRESENTATION_ITEM ( '' )  );
#11300=AXIS2_PLACEMENT_3D ( 'NONE', #7256, #3217, #21257 ) ;
#11408=( BOUNDED_CURVE ( )  B_SPLINE_CURVE ( 2, ( #7664, #11142, #16329 ),
 .UNSPECIFIED., .F., .F. ) 
 B_SPLINE_CURVE_WITH_KNOTS ( ( 3, 3 ),
 ( 0.000000000000000000, 0.1168436138077985215 ),
 .UNSPECIFIED. ) 
 CURVE ( )  GEOMETRIC_REPRESENTATION_ITEM ( )  RATIONAL_B_SPLINE_CURVE ( ( 1.000000000000000000, 1.077350269189633725, 1.077350269189629950 ) ) 
 REPRESENTATION_ITEM ( '' )  );
#11432=CARTESIAN_POINT ( 'NONE',  ( 39.37089837072279863, 22.23982225285499936, -13.00000000000049916 ) ) ;
#11522=ORIENTED_EDGE ( 'NONE', *, *, #15651, .T. ) ;
#11593=ADVANCED_FACE ( 'NONE', ( #5346 ), #22074, .T. ) ;
#11618=LINE ( 'NONE', #8150, #14523 ) ;
#11675=VECTOR ( 'NONE', #1689, 1000.000000000000000 ) ;
#11721=ORIENTED_EDGE ( 'NONE', *, *, #9493, .T. ) ;
#11796=CARTESIAN_POINT ( 'NONE',  ( 39.87324790931398866, 24.79279012203729948, -13.00000000000049916 ) ) ;
#11805=ADVANCED_FACE ( 'NONE', ( #15671 ), #22545, .T. ) ;
#11813=EDGE_LOOP ( 'NONE', ( #16697, #1032 ) ) ;
#11835=DIRECTION ( 'NONE',  ( 0.9730401042858035643, -0.2306359803922028717, -5.959266323858667582E-17 ) ) ;
#11997=CARTESIAN_POINT ( 'NONE',  ( 34.14207834813670672, 22.29249582057180135, -15.00000000000049916 ) ) ;
#12022=DIRECTION ( 'NONE',  ( -9.594916218540590128E-33, 2.583840697242805182E-16, -1.000000000000000000 ) ) ;
#12104=EDGE_LOOP ( 'NONE', ( #8068, #9636 ) ) ;
#12106=FACE_OUTER_BOUND ( 'NONE', #10957, .T. ) ;
#12220=ORIENTED_EDGE ( 'NONE', *, *, #14700, .T. ) ;
#12321=CARTESIAN_POINT ( 'NONE',  ( 37.37362508103680625, 25.08661566644150298, -13.00000000000049916 ) ) ;
#12356=EDGE_CURVE ( 'NONE', #2561, #11172, #12877, .T. ) ;
#12357=CARTESIAN_POINT ( 'NONE',  ( 49.97703550743810297, 19.72589006657999988, -15.50000000000049916 ) ) ;
#12375=PLANE ( 'NONE',  #6467 ) ;
#12440=ORIENTED_EDGE ( 'NONE', *, *, #7362, .T. ) ;
#12448=CONICAL_SURFACE ( 'NONE', #14332, 2.254620000000000513, 0.7853981633974461696 ) ;
#12477=PLANE ( 'NONE',  #19954 ) ;
#12504=PRODUCT_DEFINITION ( 'UNKNOWN', '', #1510, #12775 ) ;
#12515=LINE ( 'NONE', #19748, #11675 ) ;
#12516=FACE_OUTER_BOUND ( 'NONE', #16495, .T. ) ;
#12611=ORIENTED_EDGE ( 'NONE', *, *, #10690, .T. ) ;
#12720=DIRECTION ( 'NONE',  ( -0.9730401042858036753, 0.2306359803922028995, 5.959266323858677443E-17 ) ) ;
#12739=AXIS2_PLACEMENT_3D ( 'NONE', #2569, #13380, #415 ) ;
#12757=ORIENTED_EDGE ( 'NONE', *, *, #18960, .T. ) ;
#12768=DIRECTION ( 'NONE',  ( -0.9730401042858036753, 0.2306359803922028995, 5.959266323858677443E-17 ) ) ;
#12773=CARTESIAN_POINT ( 'NONE',  ( 36.57467860885130051, 21.71590586959130320, -11.00000000000049916 ) ) ;
#12775=DESIGN_CONTEXT ( 'detailed design', #13979, 'design' ) ;
#12776=CARTESIAN_POINT ( 'NONE',  ( 36.89121352362743522, 22.27682603178732279, -15.00000000000051514 ) ) ;
#12784=ORIENTED_EDGE ( 'NONE', *, *, #12356, .F. ) ;
#12827=ORIENTED_EDGE ( 'NONE', *, *, #8370, .T. ) ;
#12877=LINE ( 'NONE', #5517, #16986 ) ;
#12894=EDGE_CURVE ( 'NONE', #2368, #3573, #9433, .T. ) ;
#12898=CARTESIAN_POINT ( 'NONE',  ( 58.49563186522070168, 17.70675969991879839, -13.00000000000049916 ) ) ;
#12972=ADVANCED_FACE ( 'NONE', ( #5846 ), #18444, .T. ) ;
#12978=ORIENTED_EDGE ( 'NONE', *, *, #9493, .F. ) ;
#12992=DIRECTION ( 'NONE',  ( 0.9730401042858036753, -0.2306359803922031493, -5.959266323858673745E-17 ) ) ;
#13103=ORIENTED_EDGE ( 'NONE', *, *, #6234, .T. ) ;
#13127=LINE ( 'NONE', #4557, #5735 ) ;
#13150=ORIENTED_EDGE ( 'NONE', *, *, #4480, .T. ) ;
#13163=CIRCLE ( 'NONE', #20746, 4.250000000000001776 ) ;
#13179=DIRECTION ( 'NONE',  ( 0.000000000000000000, 0.000000000000000000, -1.000000000000000000 ) ) ;
#13182=AXIS2_PLACEMENT_3D ( 'NONE', #17015, #6442, #6579 ) ;
#13186=DIRECTION ( 'NONE',  ( 0.000000000000000000, 0.000000000000000000, -1.000000000000000000 ) ) ;
#13211=DIRECTION ( 'NONE',  ( 0.000000000000000000, 0.000000000000000000, 1.000000000000000000 ) ) ;
#13225=EDGE_LOOP ( 'NONE', ( #6802, #11522, #11206, #7045 ) ) ;
#13266=EDGE_LOOP ( 'NONE', ( #15423, #5822, #20018, #13569, #9217 ) ) ;
#13312=DIRECTION ( 'NONE',  ( -0.9730401042858035643, 0.2306359803922028717, 6.126766849694256332E-17 ) ) ;
#13380=DIRECTION ( 'NONE',  ( 0.000000000000000000, 0.000000000000000000, 1.000000000000000000 ) ) ;
#13385=DIRECTION ( 'NONE',  ( -0.2306359803922028995, -0.9730401042858036753, 1.343075398093749487E-16 ) ) ;
#13391=DIRECTION ( 'NONE',  ( 1.000000000000000000, 0.000000000000000000, 0.000000000000000000 ) ) ;
#13408=ORIENTED_EDGE ( 'NONE', *, *, #8870, .T. ) ;
#13430=ORIENTED_EDGE ( 'NONE', *, *, #11185, .T. ) ;
#13509=EDGE_LOOP ( 'NONE', ( #3040, #18979, #12611, #1402 ) ) ;
#13554=ORIENTED_EDGE ( 'NONE', *, *, #16902, .F. ) ;
#13569=ORIENTED_EDGE ( 'NONE', *, *, #1383, .T. ) ;
#13587=DIRECTION ( 'NONE',  ( -0.6880432561069586006, 0.1630842657209346236, 0.7071067811865459074 ) ) ;
#13590=DIRECTION ( 'NONE',  ( -0.9286452767786568252, -1.871119812896369614E-17, -0.3709689338970204586 ) ) ;
#13656=ORIENTED_EDGE ( 'NONE', *, *, #10435, .T. ) ;
#13667=MECHANICAL_CONTEXT ( 'NONE', #15946, 'mechanical' ) ;
#13714=ORIENTED_EDGE ( 'NONE', *, *, #21146, .T. ) ;
#13740=TOROIDAL_SURFACE ( 'NONE', #15243, 2.600000000000000089, 0.1000000000000000056 ) ;
#13746=ORIENTED_EDGE ( 'NONE', *, *, #14700, .F. ) ;
#13788=CARTESIAN_POINT ( 'NONE',  ( 36.84099409957970295, 22.83947580187469839, -8.750000000000499156 ) ) ;
#13885=CARTESIAN_POINT ( 'NONE',  ( 34.94102482032229773, 25.66320561742200113, -13.00000000000049916 ) ) ;
#13911=EDGE_CURVE ( 'NONE', #928, #18213, #13959, .T. ) ;
#13930=CARTESIAN_POINT ( 'NONE',  ( 34.89491389100810181, 23.30074776265910330, -8.750000000000499156 ) ) ;
#13931=CIRCLE ( 'NONE', #10154, 2.009240000000000581 ) ;
#13959=( BOUNDED_CURVE ( )  B_SPLINE_CURVE ( 2, ( #12773, #20010, #20124 ),
 .UNSPECIFIED., .F., .F. ) 
 B_SPLINE_CURVE_WITH_KNOTS ( ( 3, 3 ),
 ( 0.000000000000000000, 0.1168436138077847686 ),
 .UNSPECIFIED. ) 
 CURVE ( )  GEOMETRIC_REPRESENTATION_ITEM ( )  RATIONAL_B_SPLINE_CURVE ( ( 1.000000000000000000, 1.077350269189619514, 1.077350269189624843 ) ) 
 REPRESENTATION_ITEM ( '' )  );
#13979=APPLICATION_CONTEXT ( 'configuration controlled 3d designs of mechanical parts and assemblies' ) ;
#14033=ORIENTED_EDGE ( 'NONE', *, *, #10182, .F. ) ;
#14079=CARTESIAN_POINT ( 'NONE',  ( 37.10730959030829723, 23.96304573415810069, -11.00000000000049916 ) ) ;
#14081=ORIENTED_EDGE ( 'NONE', *, *, #12356, .T. ) ;
#14162=EDGE_CURVE ( 'NONE', #815, #886, #4053, .T. ) ;
#14179=CARTESIAN_POINT ( 'NONE',  ( 39.37089837072279863, 22.23982225285499936, -13.00000000000049916 ) ) ;
#14198=AXIS2_PLACEMENT_3D ( 'NONE', #736, #15247, #6235 ) ;
#14283=DIRECTION ( 'NONE',  ( 0.000000000000000000, 0.000000000000000000, 1.000000000000000000 ) ) ;
#14302=VECTOR ( 'NONE', #12720, 999.9999999999998863 ) ;
#14317=AXIS2_PLACEMENT_3D ( 'NONE', #16727, #18782, #13186 ) ;
#14332=AXIS2_PLACEMENT_3D ( 'NONE', #12898, #4224, #16924 ) ;
#14402=EDGE_CURVE ( 'NONE', #23420, #11102, #13163, .T. ) ;
#14403=EDGE_CURVE ( 'NONE', #19293, #8770, #12515, .T. ) ;
#14501=AXIS2_PLACEMENT_3D ( 'NONE', #21096, #22985, #3046 ) ;
#14523=VECTOR ( 'NONE', #22726, 999.9999999999998863 ) ;
#14525=DIRECTION ( 'NONE',  ( 0.000000000000000000, 0.000000000000000000, -1.000000000000000000 ) ) ;
#14700=EDGE_CURVE ( 'NONE', #5938, #2368, #2179, .T. ) ;
#14730=VERTEX_POINT ( 'NONE', #11796 ) ;
#14735=CARTESIAN_POINT ( 'NONE',  ( 36.76586756491558816, 21.07724224331880336, -14.00000000000048672 ) ) ;
#14763=EDGE_LOOP ( 'NONE', ( #7932, #13408, #16916, #12757, #12827, #16839 ) ) ;
#14791=CARTESIAN_POINT ( 'NONE',  ( 58.73439644601031517, 17.65016624305016890, -10.99076000000046172 ) ) ;
#14805=FACE_OUTER_BOUND ( 'NONE', #15804, .T. ) ;
#14856=CARTESIAN_POINT ( 'NONE',  ( 34.89491389100810181, 23.30074776265909975, -13.00000000000049916 ) ) ;
#14877=ORIENTED_EDGE ( 'NONE', *, *, #15269, .T. ) ;
#14912=DIRECTION ( 'NONE',  ( 0.000000000000000000, 0.000000000000000000, 1.000000000000000000 ) ) ;
#14915=CARTESIAN_POINT ( 'NONE',  ( 34.14207834813670672, 22.29249582057180135, -11.00000000000049916 ) ) ;
#14921=VECTOR ( 'NONE', #13385, 999.9999999999998863 ) ;
#14997=EDGE_CURVE ( 'NONE', #9786, #23152, #6909, .T. ) ;
#15023=ORIENTED_EDGE ( 'NONE', *, *, #19416, .F. ) ;
#15034=ADVANCED_FACE ( 'NONE', ( #16382 ), #21504, .T. ) ;
#15035=ORIENTED_EDGE ( 'NONE', *, *, #14403, .T. ) ;
#15061=CIRCLE ( 'NONE', #5196, 2.600000000000000089 ) ;
#15090=CARTESIAN_POINT ( 'NONE',  ( 37.48968750243700043, 22.68571848161319693, -13.00000000000049916 ) ) ;
#15128=FACE_OUTER_BOUND ( 'NONE', #16087, .T. ) ;
#15148=ORIENTED_EDGE ( 'NONE', *, *, #7751, .F. ) ;
#15186=CARTESIAN_POINT ( 'NONE',  ( 35.75979881747886679, 26.94964815373086608, -13.00000000000049916 ) ) ;
#15243=AXIS2_PLACEMENT_3D ( 'NONE', #14179, #4914, #3008 ) ;
#15247=DIRECTION ( 'NONE',  ( -0.9730401042858035643, 0.2306359803922028717, 5.432877459303547053E-17 ) ) ;
#15261=AXIS2_PLACEMENT_3D ( 'NONE', #6351, #11835, #14912 ) ;
#15265=CARTESIAN_POINT ( 'NONE',  ( 36.57467860885130051, 21.71590586959130320, -11.00000000000049916 ) ) ;
#15269=EDGE_CURVE ( 'NONE', #5418, #5938, #18669, .T. ) ;
#15399=ORIENTED_EDGE ( 'NONE', *, *, #15469, .T. ) ;
#15423=ORIENTED_EDGE ( 'NONE', *, *, #15269, .F. ) ;
#15437=CARTESIAN_POINT ( 'NONE',  ( 34.14207834813670672, 22.29249582057180135, -15.00000000000049916 ) ) ;
#15462=CARTESIAN_POINT ( 'NONE',  ( 36.76586756491560237, 21.07724224331881047, -12.00000000000050093 ) ) ;
#15469=EDGE_CURVE ( 'NONE', #23382, #3254, #16242, .T. ) ;
#15471=AXIS2_PLACEMENT_3D ( 'NONE', #21120, #6523, #8428 ) ;
#15479=( BOUNDED_CURVE ( )  B_SPLINE_CURVE ( 2, ( #21545, #12776, #22014 ),
 .UNSPECIFIED., .F., .F. ) 
 B_SPLINE_CURVE_WITH_KNOTS ( ( 3, 3 ),
 ( 0.1168436138077985215, 0.2336872276155859962 ),
 .UNSPECIFIED. ) 
 CURVE ( )  GEOMETRIC_REPRESENTATION_ITEM ( )  RATIONAL_B_SPLINE_CURVE ( ( 1.077350269189629950, 1.077350269189626175, 1.000000000000000000 ) ) 
 REPRESENTATION_ITEM ( '' )  );
#15511=DIRECTION ( 'NONE',  ( 5.798605125234323991E-17, -1.374421231021384554E-17, 1.000000000000000000 ) ) ;
#15519=ORIENTED_EDGE ( 'NONE', *, *, #4469, .T. ) ;
#15537=LINE ( 'NONE', #19228, #6710 ) ;
#15542=DIRECTION ( 'NONE',  ( -0.9730401042858036753, 0.2306359803922028995, 5.959266323858677443E-17 ) ) ;
#15609=CARTESIAN_POINT ( 'NONE',  ( 37.37362508103680625, 25.08661566644150298, -13.00000000000049916 ) ) ;
#15651=EDGE_CURVE ( 'NONE', #886, #3254, #5660, .T. ) ;
#15671=FACE_OUTER_BOUND ( 'NONE', #17581, .T. ) ;
#15728=ORIENTED_EDGE ( 'NONE', *, *, #19416, .T. ) ;
#15782=ADVANCED_FACE ( 'NONE', ( #10055 ), #13740, .F. ) ;
#15804=EDGE_LOOP ( 'NONE', ( #18247, #14081, #750, #7785 ) ) ;
#15908=EDGE_CURVE ( 'NONE', #17960, #22329, #19881, .T. ) ;
#15946=APPLICATION_CONTEXT ( 'configuration controlled 3d designs of mechanical parts and assemblies' ) ;
#15985=FACE_BOUND ( 'NONE', #19821, .T. ) ;
#16076=DIRECTION ( 'NONE',  ( -0.9730401042858035643, 0.2306359803922028717, 5.959266323858677443E-17 ) ) ;
#16082=CARTESIAN_POINT ( 'NONE',  ( 38.13838090529419844, 22.53196116135175231, -13.00000000000049916 ) ) ;
#16087=EDGE_LOOP ( 'NONE', ( #6533, #17751, #3794, #5096 ) ) ;
#16147=ORIENTED_EDGE ( 'NONE', *, *, #12894, .T. ) ;
#16179=CARTESIAN_POINT ( 'NONE',  ( 39.27359436029429673, 22.26288585089420025, -13.00000000000049916 ) ) ;
#16242=LINE ( 'NONE', #12357, #20164 ) ;
#16260=CARTESIAN_POINT ( 'NONE',  ( 37.13840842239409312, 23.31972727237320342, -11.00000000000049738 ) ) ;
#16292=CARTESIAN_POINT ( 'NONE',  ( 58.73439644601030096, 17.65016624305009785, -13.00000000000049916 ) ) ;
#16329=CARTESIAN_POINT ( 'NONE',  ( 37.01481097301077483, 22.79827665208023646, -15.00000000000051159 ) ) ;
#16348=EDGE_LOOP ( 'NONE', ( #6860, #767, #1271, #7566, #3200 ) ) ;
#16377=SHAPE_REPRESENTATION_RELATIONSHIP ( 'NONE' , 'NONE' ,  #22194, #16713 ) ;
#16382=FACE_OUTER_BOUND ( 'NONE', #13225, .T. ) ;
#16391=ORIENTED_EDGE ( 'NONE', *, *, #2974, .T. ) ;
#16443=CARTESIAN_POINT ( 'NONE',  ( 39.37089837072279863, 22.23982225285499936, -13.00000000000049916 ) ) ;
#16495=EDGE_LOOP ( 'NONE', ( #4940, #2765, #22156, #12784, #17236 ) ) ;
#16588=EDGE_LOOP ( 'NONE', ( #19220, #19788, #16750, #15148, #13746 ) ) ;
#16647=CARTESIAN_POINT ( 'NONE',  ( 34.40839383886520153, 23.41606575285519654, -13.00000000000049916 ) ) ;
#16670=LINE ( 'NONE', #22144, #5322 ) ;
#16693=AXIS2_PLACEMENT_3D ( 'NONE', #21967, #3803, #11083 ) ;
#16697=ORIENTED_EDGE ( 'NONE', *, *, #14402, .T. ) ;
#16713=ADVANCED_BREP_SHAPE_REPRESENTATION ( '', ( #9848, #12739 ), #5684 ) ;
#16727=CARTESIAN_POINT ( 'NONE',  ( 49.97703550743810297, 19.72589006657999988, -13.00000000000049916 ) ) ;
#16750=ORIENTED_EDGE ( 'NONE', *, *, #14402, .F. ) ;
#16839=ORIENTED_EDGE ( 'NONE', *, *, #5400, .T. ) ;
#16902=EDGE_CURVE ( 'NONE', #928, #20160, #22547, .T. ) ;
#16916=ORIENTED_EDGE ( 'NONE', *, *, #8037, .T. ) ;
#16924=DIRECTION ( 'NONE',  ( 0.000000000000000000, 0.000000000000000000, 1.000000000000000000 ) ) ;
#16930=AXIS2_PLACEMENT_3D ( 'NONE', #20091, #19749, #19982 ) ;
#16986=VECTOR ( 'NONE', #12768, 999.9999999999998863 ) ;
#17015=CARTESIAN_POINT ( 'NONE',  ( 34.89491389100810181, 23.30074776265909975, -13.00000000000049916 ) ) ;
#17023=FACE_OUTER_BOUND ( 'NONE', #17553, .T. ) ;
#17076=DIRECTION ( 'NONE',  ( 0.9730401042858035643, -0.2306359803922028717, -5.432877459303547053E-17 ) ) ;
#17147=AXIS2_PLACEMENT_3D ( 'NONE', #7782, #879, #13590 ) ;
#17193=EDGE_CURVE ( 'NONE', #22740, #3573, #8873, .T. ) ;
#17227=EDGE_CURVE ( 'NONE', #22935, #18764, #2792, .T. ) ;
#17236=ORIENTED_EDGE ( 'NONE', *, *, #8037, .F. ) ;
#17244=FACE_OUTER_BOUND ( 'NONE', #17282, .T. ) ;
#17282=EDGE_LOOP ( 'NONE', ( #5553, #20435, #12978, #23351 ) ) ;
#17356=AXIS2_PLACEMENT_3D ( 'NONE', #1584, #7184, #10771 ) ;
#17362=CARTESIAN_POINT ( 'NONE',  ( 36.57467860885130051, 21.71590586959130320, -15.00000000000049916 ) ) ;
#17416=CARTESIAN_POINT ( 'NONE',  ( 36.30836311812279860, 20.59233593730780143, -13.00000000000049916 ) ) ;
#17553=EDGE_LOOP ( 'NONE', ( #2525, #15035, #13656, #13714, #13103, #19690 ) ) ;
#17581=EDGE_LOOP ( 'NONE', ( #23288, #22044, #4944, #7662, #19269 ) ) ;
#17595=CIRCLE ( 'NONE', #5777, 2.500000000000000444 ) ;
#17637=PRODUCT_DEFINITION_SHAPE ( 'NONE', 'NONE',  #12504 ) ;
#17703=DIRECTION ( 'NONE',  ( 0.9730401042858036753, -0.2306359803922028995, -5.432877459303547669E-17 ) ) ;
#17712=DIRECTION ( 'NONE',  ( 0.9730401042858036753, -0.2306359803922028995, -5.432877459303547669E-17 ) ) ;
#17729=AXIS2_PLACEMENT_3D ( 'NONE', #8139, #23064, #22950 ) ;
#17735=CIRCLE ( 'NONE', #13182, 4.250000000000000000 ) ;
#17751=ORIENTED_EDGE ( 'NONE', *, *, #15908, .F. ) ;
#17785=VERTEX_POINT ( 'NONE', #9755 ) ;
#17823=CARTESIAN_POINT ( 'NONE',  ( 34.67470932959370344, 24.53963568513860238, -11.00000000000049916 ) ) ;
#17860=ORIENTED_EDGE ( 'NONE', *, *, #18810, .F. ) ;
#17903=CARTESIAN_POINT ( 'NONE',  ( 39.37089837072280574, 22.23982225285502068, -15.50000000000049916 ) ) ;
#17919=CIRCLE ( 'NONE', #9590, 2.500000000000000444 ) ;
#17935=AXIS2_PLACEMENT_3D ( 'NONE', #8754, #23231, #5185 ) ;
#17960=VERTEX_POINT ( 'NONE', #13885 ) ;
#18070=ORIENTED_EDGE ( 'NONE', *, *, #23017, .F. ) ;
#18084=CARTESIAN_POINT ( 'NONE',  ( 34.07549947545459901, 22.01160333750090459, -14.50000000000050093 ) ) ;
#18110=AXIS2_PLACEMENT_3D ( 'NONE', #20222, #21143, #6312 ) ;
#18203=DIRECTION ( 'NONE',  ( 0.9730401042858036753, -0.2306359803922028995, -5.959266323858677443E-17 ) ) ;
#18213=VERTEX_POINT ( 'NONE', #20400 ) ;
#18247=ORIENTED_EDGE ( 'NONE', *, *, #18960, .F. ) ;
#18365=CARTESIAN_POINT ( 'NONE',  ( 38.67394081127452665, 19.73298157975111877, -13.00000000000049916 ) ) ;
#18391=CARTESIAN_POINT ( 'NONE',  ( 35.09206298776550170, 20.88063091279809669, -13.00000000000049916 ) ) ;
#18412=CARTESIAN_POINT ( 'NONE',  ( 33.54350891239443655, 19.76716536178343731, -13.00000000000049916 ) ) ;
#18413=( NAMED_UNIT ( * ) PLANE_ANGLE_UNIT ( ) SI_UNIT ( $, .RADIAN. ) );
#18428=DIRECTION ( 'NONE',  ( 0.9730401042858035643, -0.2306359803922028717, -5.432877459303547053E-17 ) ) ;
#18431=ADVANCED_FACE ( 'NONE', ( #15985, #22879 ), #6990, .T. ) ;
#18444=CYLINDRICAL_SURFACE ( 'NONE', #682, 4.250000000000001776 ) ;
#18453=DIRECTION ( 'NONE',  ( -0.9730401042858035643, 0.2306359803922028717, 6.126766849694256332E-17 ) ) ;
#18482=CARTESIAN_POINT ( 'NONE',  ( 35.27327876533596651, 27.06496614392695932, -13.00000000000049916 ) ) ;
#18567=ADVANCED_FACE ( 'NONE', ( #20986 ), #20019, .F. ) ;
#18599=EDGE_LOOP ( 'NONE', ( #616, #13150, #21407, #13430, #14033 ) ) ;
#18650=ORIENTED_EDGE ( 'NONE', *, *, #6517, .T. ) ;
#18669=CIRCLE ( 'NONE', #4616, 0.5000000000000004441 ) ;
#18764=VERTEX_POINT ( 'NONE', #8987 ) ;
#18782=DIRECTION ( 'NONE',  ( 0.9730401042858035643, -0.2306359803922028717, -5.432877459303547053E-17 ) ) ;
#18810=EDGE_CURVE ( 'NONE', #3926, #14730, #19825, .T. ) ;
#18840=CONICAL_SURFACE ( 'NONE', #217, 1.154700538379250796, 1.047197551196598297 ) ;
#18860=EDGE_LOOP ( 'NONE', ( #9736, #9972, #2034, #15399, #18070 ) ) ;
#18878=CARTESIAN_POINT ( 'NONE',  ( 58.25686728443099582, 17.76335315678740301, -13.00000000000049916 ) ) ;
#18905=FACE_OUTER_BOUND ( 'NONE', #14763, .T. ) ;
#18960=EDGE_CURVE ( 'NONE', #2561, #22329, #7787, .T. ) ;
#18979=ORIENTED_EDGE ( 'NONE', *, *, #10961, .T. ) ;
#18986=EDGE_CURVE ( 'NONE', #20160, #483, #21182, .T. ) ;
#19063=AXIS2_PLACEMENT_3D ( 'NONE', #5699, #19860, #3462 ) ;
#19165=CARTESIAN_POINT ( 'NONE',  ( 36.57467860885130051, 21.71590586959130320, -11.00000000000049916 ) ) ;
#19219=CARTESIAN_POINT ( 'NONE',  ( 37.56481403710107969, 24.44795204016911327, -14.00000000000048672 ) ) ;
#19220=ORIENTED_EDGE ( 'NONE', *, *, #1040, .F. ) ;
#19228=CARTESIAN_POINT ( 'NONE',  ( 34.87444594764010475, 25.38231313435120029, -13.50000000000049916 ) ) ;
#19269=ORIENTED_EDGE ( 'NONE', *, *, #4469, .F. ) ;
#19293=VERTEX_POINT ( 'NONE', #16082 ) ;
#19416=EDGE_CURVE ( 'NONE', #23152, #3517, #505, .T. ) ;
#19419=DIRECTION ( 'NONE',  ( 0.000000000000000000, 0.000000000000000000, 1.000000000000000000 ) ) ;
#19622=CIRCLE ( 'NONE', #21878, 3.750000000000000000 ) ;
#19690=ORIENTED_EDGE ( 'NONE', *, *, #13911, .T. ) ;
#19717=AXIS2_PLACEMENT_3D ( 'NONE', #20314, #18428, #7493 ) ;
#19743=AXIS2_PLACEMENT_3D ( 'NONE', #9724, #15511, #13391 ) ;
#19748=CARTESIAN_POINT ( 'NONE',  ( 37.48968750243700043, 22.68571848161319693, -14.15470053837974973 ) ) ;
#19749=DIRECTION ( 'NONE',  ( 1.040345436475888435E-32, 1.169424102322700040E-16, 1.000000000000000000 ) ) ;
#19788=ORIENTED_EDGE ( 'NONE', *, *, #6695, .T. ) ;
#19821=EDGE_LOOP ( 'NONE', ( #15728, #16391, #8409, #4952, #9789, #11721 ) ) ;
#19825=CIRCLE ( 'NONE', #15261, 2.600000000000000089 ) ;
#19860=DIRECTION ( 'NONE',  ( -8.623081276789554834E-17, -1.054188326053478339E-16, -1.000000000000000000 ) ) ;
#19881=LINE ( 'NONE', #3480, #22445 ) ;
#19954=AXIS2_PLACEMENT_3D ( 'NONE', #21246, #8569, #12022 ) ;
#19982=DIRECTION ( 'NONE',  ( 1.000000000000000000, -8.896220237034308570E-17, 0.000000000000000000 ) ) ;
#20010=CARTESIAN_POINT ( 'NONE',  ( 36.89121352362742101, 22.27682603178731924, -11.00000000000049738 ) ) ;
#20014=DIRECTION ( 'NONE',  ( 5.798605125234323991E-17, -1.374421231021384554E-17, 1.000000000000000000 ) ) ;
#20018=ORIENTED_EDGE ( 'NONE', *, *, #17193, .T. ) ;
#20019=PLANE ( 'NONE',  #1231 ) ;
#20088=DIRECTION ( 'NONE',  ( 0.1153179901961009640, 0.4865200521429018377, -0.8660254037844385966 ) ) ;
#20089=DIRECTION ( 'NONE',  ( 0.9730401042858036753, -0.2306359803922031493, -5.432877459303553216E-17 ) ) ;
#20091=CARTESIAN_POINT ( 'NONE',  ( 34.14207834813670672, 22.29249582057180135, -11.00000000000049916 ) ) ;
#20124=CARTESIAN_POINT ( 'NONE',  ( 37.01481097301073930, 22.79827665208023291, -11.00000000000049560 ) ) ;
#20133=ADVANCED_FACE ( 'NONE', ( #12106 ), #6185, .T. ) ;
#20160=VERTEX_POINT ( 'NONE', #14915 ) ;
#20164=VECTOR ( 'NONE', #1505, 999.9999999999998863 ) ;
#20222=CARTESIAN_POINT ( 'NONE',  ( 34.89491389100810181, 23.30074776265909975, -13.00000000000049916 ) ) ;
#20285=DIRECTION ( 'NONE',  ( -0.6880432561069586006, 0.1630842657209347069, -0.7071067811865459074 ) ) ;
#20286=DIRECTION ( 'NONE',  ( -0.9730401042858036753, 0.2306359803922028995, 5.959266323858677443E-17 ) ) ;
#20314=CARTESIAN_POINT ( 'NONE',  ( 58.25686728443099582, 17.76335315678740301, -13.00000000000049916 ) ) ;
#20327=DIRECTION ( 'NONE',  ( 0.9730401042858035643, -0.2306359803922028717, -5.432877459303547053E-17 ) ) ;
#20333=DIRECTION ( 'NONE',  ( 0.9730401042858035643, -0.2306359803922028717, -5.959266323858667582E-17 ) ) ;
#20400=CARTESIAN_POINT ( 'NONE',  ( 37.01481097301073930, 22.79827665208023291, -11.00000000000049560 ) ) ;
#20411=EDGE_CURVE ( 'NONE', #17785, #3517, #11618, .T. ) ;
#20435=ORIENTED_EDGE ( 'NONE', *, *, #14997, .T. ) ;
#20442=DIRECTION ( 'NONE',  ( 0.000000000000000000, 0.000000000000000000, -1.000000000000000000 ) ) ;
#20635=CARTESIAN_POINT ( 'NONE',  ( 33.91471097434123294, 19.16532731944443313, -13.00000000000049916 ) ) ;
#20672=DIRECTION ( 'NONE',  ( -0.9730401042858035643, 0.2306359803922028717, 5.432877459303547053E-17 ) ) ;
#20746=AXIS2_PLACEMENT_3D ( 'NONE', #16179, #20089, #14525 ) ;
#20799=CARTESIAN_POINT ( 'NONE',  ( 39.27359436029429673, 22.26288585089420025, -13.00000000000049916 ) ) ;
#20807=CARTESIAN_POINT ( 'NONE',  ( 34.54155158422950223, 23.97785071899690124, -15.00000000000049916 ) ) ;
#20855=DIRECTION ( 'NONE',  ( 0.9730401042858035643, -0.2306359803922028717, -5.959266323858677443E-17 ) ) ;
#20890=ORIENTED_EDGE ( 'NONE', *, *, #18810, .T. ) ;
#20916=DIRECTION ( 'NONE',  ( -9.594916218540590128E-33, 2.583840697242805182E-16, -1.000000000000000000 ) ) ;
#20944=VECTOR ( 'NONE', #17703, 999.9999999999998863 ) ;
#20975=CARTESIAN_POINT ( 'NONE',  ( 37.01481097301077483, 22.79827665208023646, -15.00000000000051159 ) ) ;
#20986=FACE_OUTER_BOUND ( 'NONE', #1166, .T. ) ;
#21096=CARTESIAN_POINT ( 'NONE',  ( 34.40839383886520153, 23.41606575285519654, -16.27970053837979947 ) ) ;
#21120=CARTESIAN_POINT ( 'NONE',  ( 49.97703550743810297, 19.72589006657999988, -13.00000000000049916 ) ) ;
#21143=DIRECTION ( 'NONE',  ( -0.9730401042858036753, 0.2306359803922031493, 5.432877459303543355E-17 ) ) ;
#21146=EDGE_CURVE ( 'NONE', #9786, #8780, #6263, .T. ) ;
#21182=LINE ( 'NONE', #1459, #5787 ) ;
#21225=ORIENTED_EDGE ( 'NONE', *, *, #10435, .F. ) ;
#21246=CARTESIAN_POINT ( 'NONE',  ( 58.73439644601030096, 17.65016624305009785, -14.25000000000050093 ) ) ;
#21257=DIRECTION ( 'NONE',  ( 0.000000000000000000, 0.000000000000000000, 1.000000000000000000 ) ) ;
#21264=FACE_OUTER_BOUND ( 'NONE', #11813, .T. ) ;
#21407=ORIENTED_EDGE ( 'NONE', *, *, #6344, .T. ) ;
#21504=CONICAL_SURFACE ( 'NONE', #11300, 2.254620000000000513, 0.7853981633974461696 ) ;
#21526=CARTESIAN_POINT ( 'NONE',  ( 35.87511680767496358, 27.43616820587376637, -13.00000000000049916 ) ) ;
#21545=CARTESIAN_POINT ( 'NONE',  ( 37.01481097301077483, 22.79827665208023646, -15.00000000000051159 ) ) ;
#21878=AXIS2_PLACEMENT_3D ( 'NONE', #16647, #12992, #7764 ) ;
#21902=DIRECTION ( 'NONE',  ( -0.9730401042858035643, 0.2306359803922028717, 6.126766849694256332E-17 ) ) ;
#21907=CARTESIAN_POINT ( 'NONE',  ( 33.87576285740820481, 21.16892588828840260, -13.00000000000049916 ) ) ;
#21967=CARTESIAN_POINT ( 'NONE',  ( 39.27359436029429673, 22.26288585089420025, -13.00000000000049916 ) ) ;
#22014=CARTESIAN_POINT ( 'NONE',  ( 36.57467860885130051, 21.71590586959130320, -15.00000000000049916 ) ) ;
#22044=ORIENTED_EDGE ( 'NONE', *, *, #22553, .T. ) ;
#22074=CYLINDRICAL_SURFACE ( 'NONE', #14317, 2.500000000000000444 ) ;
#22087=DIRECTION ( 'NONE',  ( 0.000000000000000000, 0.000000000000000000, 1.000000000000000000 ) ) ;
#22101=DIRECTION ( 'NONE',  ( -0.9730401042858036753, 0.2306359803922031493, 5.432877459303543355E-17 ) ) ;
#22113=DIRECTION ( 'NONE',  ( 0.000000000000000000, 0.000000000000000000, 1.000000000000000000 ) ) ;
#22144=CARTESIAN_POINT ( 'NONE',  ( 34.74128820227589642, 24.82052816820949914, -11.50000000000049916 ) ) ;
#22156=ORIENTED_EDGE ( 'NONE', *, *, #8689, .F. ) ;
#22181=( NAMED_UNIT ( * ) SI_UNIT ( $, .STERADIAN. ) SOLID_ANGLE_UNIT ( ) );
#22194=SHAPE_REPRESENTATION ( '1602p_c_43', ( #12739 ), #5684 ) ;
#22326=CARTESIAN_POINT ( 'NONE',  ( 36.84099409957970295, 22.83947580187469839, -13.00000000000049916 ) ) ;
#22329=VERTEX_POINT ( 'NONE', #12321 ) ;
#22334=DIRECTION ( 'NONE',  ( 0.000000000000000000, 0.000000000000000000, 1.000000000000000000 ) ) ;
#22362=CIRCLE ( 'NONE', #1886, 4.250000000000000000 ) ;
#22396=CLOSED_SHELL ( 'NONE', ( #1865, #8132, #20133, #15034, #11805, #15782, #10097, #11593, #4583, #707, #2048, #1112, #18431, #12972, #18567, #1996, #22853, #3967, #2900, #9935, #9247 ) ) ;
#22445=VECTOR ( 'NONE', #18203, 999.9999999999998863 ) ;
#22522=FACE_OUTER_BOUND ( 'NONE', #8802, .T. ) ;
#22545=CYLINDRICAL_SURFACE ( 'NONE', #15471, 2.500000000000000444 ) ;
#22547=LINE ( 'NONE', #1043, #3146 ) ;
#22553=EDGE_CURVE ( 'NONE', #18764, #9785, #2890, .T. ) ;
#22637=EDGE_LOOP ( 'NONE', ( #17860, #11165 ) ) ;
#22674=DIRECTION ( 'NONE',  ( -0.1997366180463770735, -0.8426774492125654881, -0.4999999999999997780 ) ) ;
#22726=DIRECTION ( 'NONE',  ( -0.9730401042858036753, 0.2306359803922028995, 5.959266323858677443E-17 ) ) ;
#22740=VERTEX_POINT ( 'NONE', #18412 ) ;
#22793=DIRECTION ( 'NONE',  ( 0.000000000000000000, 0.000000000000000000, -1.000000000000000000 ) ) ;
#22846=VERTEX_POINT ( 'NONE', #13930 ) ;
#22853=ADVANCED_FACE ( 'NONE', ( #5563 ), #8593, .F. ) ;
#22879=FACE_OUTER_BOUND ( 'NONE', #7345, .T. ) ;
#22935=VERTEX_POINT ( 'NONE', #9850 ) ;
#22950=DIRECTION ( 'NONE',  ( 0.000000000000000000, 0.000000000000000000, 1.000000000000000000 ) ) ;
#22955=ORIENTED_EDGE ( 'NONE', *, *, #17193, .F. ) ;
#22985=DIRECTION ( 'NONE',  ( -0.9730401042858035643, 0.2306359803922028717, 5.959266323858679908E-17 ) ) ;
#23017=EDGE_CURVE ( 'NONE', #9785, #3254, #23319, .T. ) ;
#23064=DIRECTION ( 'NONE',  ( -0.9730401042858035643, 0.2306359803922028717, 5.959266323858677443E-17 ) ) ;
#23146=CARTESIAN_POINT ( 'NONE',  ( 35.35837847849400362, 22.00420084508149898, -15.00000000000049916 ) ) ;
#23152=VERTEX_POINT ( 'NONE', #11997 ) ;
#23158=ORIENTED_EDGE ( 'NONE', *, *, #1139, .F. ) ;
#23231=DIRECTION ( 'NONE',  ( 0.9730401042858035643, -0.2306359803922028717, -5.959266323858677443E-17 ) ) ;
#23269=CARTESIAN_POINT ( 'NONE',  ( 36.84099409957970295, 22.83947580187469839, -17.25000000000050093 ) ) ;
#23288=ORIENTED_EDGE ( 'NONE', *, *, #4480, .F. ) ;
#23319=CIRCLE ( 'NONE', #4753, 2.500000000000000444 ) ;
#23351=ORIENTED_EDGE ( 'NONE', *, *, #3286, .F. ) ;
#23382=VERTEX_POINT ( 'NONE', #17903 ) ;
#23420=VERTEX_POINT ( 'NONE', #1621 ) ;
#23423=UNCERTAINTY_MEASURE_WITH_UNIT (LENGTH_MEASURE( 1.000000000000000082E-05 ), #7374, 'distance_accuracy_value', 'NONE');
#23450=DIRECTION ( 'NONE',  ( 1.000000000000000000, 0.000000000000000000, 0.000000000000000000 ) ) ;
#23515=COLOUR_RGB('Deep Blue', 0.09019608, 0.27058824, 0.51372549);
#23516=FILL_AREA_STYLE_COLOUR('',#23515);
#23517=FILL_AREA_STYLE('',(#23516));
#23518=SURFACE_STYLE_FILL_AREA(#23517);
#23519=SURFACE_SIDE_STYLE('',(#23518));
#23520=SURFACE_STYLE_USAGE(.BOTH.,#23519);
#23521=PRESENTATION_STYLE_ASSIGNMENT((#23520));
#23611=STYLED_ITEM('',(#23521),#9848);
#23612=MECHANICAL_DESIGN_GEOMETRIC_PRESENTATION_REPRESENTATION('',(#23611),#5684);
ENDSEC;
END-ISO-10303-21;
